ISO-10303-21;
HEADER;
/* Generated by software containing ST-Developer
 * from STEP Tools, Inc. (www.steptools.com) 
 */

FILE_DESCRIPTION(
/* description */ ('Manual rail carriage with stops'),
/* implementation_level */ '2;1');

FILE_NAME(
/* name */ 'Captive slot nut.step',
/* time_stamp */ '2026-10-27T18:54:27-07:00',
/* author */ (''),
/* organization */ (''),
/* preprocessor_version */ 'ST-DEVELOPER v20.2',
/* originating_system */ 'Autodesk Translation Framework v15.17.0.0',
/* authorisation */ '');

FILE_SCHEMA (('AUTOMOTIVE_DESIGN { 1 0 10303 214 3 1 1 }'));
ENDSEC;

DATA;
#10=MECHANICAL_DESIGN_GEOMETRIC_PRESENTATION_REPRESENTATION('',(#275),#8499);
#235=ELLIPSE('',#5274,0.299389011154384,0.2117);
#236=ELLIPSE('',#5278,0.299389011154384,0.2117);
#239=SHAPE_REPRESENTATION_RELATIONSHIP('SRR','None',#8602,#257);
#257=ADVANCED_BREP_SHAPE_REPRESENTATION('',(#293),#8481);
#275=STYLED_ITEM('',(#8795),#293);
#293=MANIFOLD_SOLID_BREP('Body1',#4943);
#335=FACE_BOUND('',#942,.T.);
#432=PLANE('',#5264);
#433=PLANE('',#5265);
#434=PLANE('',#5266);
#435=PLANE('',#5268);
#436=PLANE('',#5269);
#437=PLANE('',#5270);
#438=PLANE('',#5271);
#439=PLANE('',#5272);
#440=PLANE('',#5273);
#441=PLANE('',#5280);
#442=PLANE('',#5281);
#443=PLANE('',#5282);
#444=PLANE('',#5283);
#644=FACE_OUTER_BOUND('',#939,.T.);
#645=FACE_OUTER_BOUND('',#940,.T.);
#646=FACE_OUTER_BOUND('',#941,.T.);
#647=FACE_OUTER_BOUND('',#943,.T.);
#648=FACE_OUTER_BOUND('',#944,.T.);
#649=FACE_OUTER_BOUND('',#945,.T.);
#650=FACE_OUTER_BOUND('',#946,.T.);
#651=FACE_OUTER_BOUND('',#947,.T.);
#652=FACE_OUTER_BOUND('',#948,.T.);
#653=FACE_OUTER_BOUND('',#949,.T.);
#654=FACE_OUTER_BOUND('',#950,.T.);
#655=FACE_OUTER_BOUND('',#951,.T.);
#656=FACE_OUTER_BOUND('',#952,.T.);
#657=FACE_OUTER_BOUND('',#953,.T.);
#939=EDGE_LOOP('',(#3738,#3739,#3740,#3741));
#940=EDGE_LOOP('',(#3742,#3743,#3744,#3745));
#941=EDGE_LOOP('',(#3746,#3747,#3748,#3749));
#942=EDGE_LOOP('',(#3750));
#943=EDGE_LOOP('',(#3751,#3752,#3753,#3754,#3755,#3756,#3757,#3758,#3759,
#3760));
#944=EDGE_LOOP('',(#3761,#3762,#3763,#3764));
#945=EDGE_LOOP('',(#3765,#3766,#3767,#3768));
#946=EDGE_LOOP('',(#3769,#3770,#3771,#3772,#3773,#3774,#3775,#3776,#3777,
#3778));
#947=EDGE_LOOP('',(#3779,#3780,#3781,#3782));
#948=EDGE_LOOP('',(#3783,#3784,#3785,#3786,#3787,#3788));
#949=EDGE_LOOP('',(#3789,#3790,#3791,#3792,#3793,#3794,#3795,#3796));
#950=EDGE_LOOP('',(#3797,#3798,#3799,#3800,#3801));
#951=EDGE_LOOP('',(#3802,#3803,#3804,#3805));
#952=EDGE_LOOP('',(#3806,#3807,#3808,#3809,#3810,#3811));
#953=EDGE_LOOP('',(#3812,#3813,#3814,#3815));
#1341=LINE('',#7459,#1841);
#1342=LINE('',#7461,#1842);
#1343=LINE('',#7463,#1843);
#1344=LINE('',#7464,#1844);
#1345=LINE('',#7467,#1845);
#1346=LINE('',#7469,#1846);
#1347=LINE('',#7470,#1847);
#1348=LINE('',#7473,#1848);
#1349=LINE('',#7475,#1849);
#1350=LINE('',#7476,#1850);
#1351=LINE('',#7481,#1851);
#1352=LINE('',#7483,#1852);
#1353=LINE('',#7485,#1853);
#1354=LINE('',#7487,#1854);
#1355=LINE('',#7489,#1855);
#1356=LINE('',#7491,#1856);
#1357=LINE('',#7492,#1857);
#1358=LINE('',#7495,#1858);
#1359=LINE('',#7496,#1859);
#1360=LINE('',#7499,#1860);
#1361=LINE('',#7500,#1861);
#1362=LINE('',#7503,#1862);
#1363=LINE('',#7505,#1863);
#1364=LINE('',#7507,#1864);
#1365=LINE('',#7509,#1865);
#1366=LINE('',#7510,#1866);
#1367=LINE('',#7512,#1867);
#1368=LINE('',#7515,#1868);
#1369=LINE('',#7518,#1869);
#1370=LINE('',#7522,#1870);
#1371=LINE('',#7529,#1871);
#1372=LINE('',#7531,#1872);
#1373=LINE('',#7533,#1873);
#1841=VECTOR('',#5996,1.);
#1842=VECTOR('',#5997,1.);
#1843=VECTOR('',#5998,1.);
#1844=VECTOR('',#5999,1.);
#1845=VECTOR('',#6002,1.);
#1846=VECTOR('',#6003,1.);
#1847=VECTOR('',#6004,1.);
#1848=VECTOR('',#6007,1.);
#1849=VECTOR('',#6008,1.);
#1850=VECTOR('',#6009,1.);
#1851=VECTOR('',#6014,1.);
#1852=VECTOR('',#6015,1.);
#1853=VECTOR('',#6016,1.);
#1854=VECTOR('',#6017,1.);
#1855=VECTOR('',#6018,1.);
#1856=VECTOR('',#6019,1.);
#1857=VECTOR('',#6020,1.);
#1858=VECTOR('',#6023,1.);
#1859=VECTOR('',#6024,1.);
#1860=VECTOR('',#6027,1.);
#1861=VECTOR('',#6028,1.);
#1862=VECTOR('',#6031,1.);
#1863=VECTOR('',#6032,1.);
#1864=VECTOR('',#6033,1.);
#1865=VECTOR('',#6034,1.);
#1866=VECTOR('',#6035,1.);
#1867=VECTOR('',#6038,1.);
#1868=VECTOR('',#6041,1.);
#1869=VECTOR('',#6044,1.);
#1870=VECTOR('',#6049,0.21);
#1871=VECTOR('',#6058,1.);
#1872=VECTOR('',#6061,1.);
#1873=VECTOR('',#6064,1.);
#2212=CIRCLE('',#5267,0.2117);
#2213=CIRCLE('',#5276,0.2117);
#2214=CIRCLE('',#5277,0.2117);
#2215=CIRCLE('',#5279,0.2117);
#2438=VERTEX_POINT('',#7457);
#2439=VERTEX_POINT('',#7458);
#2440=VERTEX_POINT('',#7460);
#2441=VERTEX_POINT('',#7462);
#2442=VERTEX_POINT('',#7466);
#2443=VERTEX_POINT('',#7468);
#2444=VERTEX_POINT('',#7472);
#2445=VERTEX_POINT('',#7474);
#2446=VERTEX_POINT('',#7477);
#2447=VERTEX_POINT('',#7480);
#2448=VERTEX_POINT('',#7482);
#2449=VERTEX_POINT('',#7484);
#2450=VERTEX_POINT('',#7486);
#2451=VERTEX_POINT('',#7488);
#2452=VERTEX_POINT('',#7490);
#2453=VERTEX_POINT('',#7494);
#2454=VERTEX_POINT('',#7498);
#2455=VERTEX_POINT('',#7502);
#2456=VERTEX_POINT('',#7504);
#2457=VERTEX_POINT('',#7506);
#2458=VERTEX_POINT('',#7508);
#2459=VERTEX_POINT('',#7514);
#2460=VERTEX_POINT('',#7516);
#2461=VERTEX_POINT('',#7520);
#2462=VERTEX_POINT('',#7523);
#2463=VERTEX_POINT('',#7525);
#2917=EDGE_CURVE('',#2438,#2439,#1341,.T.);
#2918=EDGE_CURVE('',#2440,#2438,#1342,.T.);
#2919=EDGE_CURVE('',#2441,#2440,#1343,.T.);
#2920=EDGE_CURVE('',#2439,#2441,#1344,.T.);
#2921=EDGE_CURVE('',#2440,#2442,#1345,.T.);
#2922=EDGE_CURVE('',#2443,#2442,#1346,.T.);
#2923=EDGE_CURVE('',#2441,#2443,#1347,.T.);
#2924=EDGE_CURVE('',#2442,#2444,#1348,.T.);
#2925=EDGE_CURVE('',#2444,#2445,#1349,.T.);
#2926=EDGE_CURVE('',#2445,#2443,#1350,.T.);
#2927=EDGE_CURVE('',#2446,#2446,#2212,.T.);
#2928=EDGE_CURVE('',#2447,#2438,#1351,.T.);
#2929=EDGE_CURVE('',#2448,#2447,#1352,.T.);
#2930=EDGE_CURVE('',#2448,#2449,#1353,.T.);
#2931=EDGE_CURVE('',#2450,#2449,#1354,.T.);
#2932=EDGE_CURVE('',#2450,#2451,#1355,.T.);
#2933=EDGE_CURVE('',#2451,#2452,#1356,.T.);
#2934=EDGE_CURVE('',#2452,#2444,#1357,.T.);
#2935=EDGE_CURVE('',#2452,#2453,#1358,.T.);
#2936=EDGE_CURVE('',#2453,#2445,#1359,.T.);
#2937=EDGE_CURVE('',#2454,#2451,#1360,.T.);
#2938=EDGE_CURVE('',#2453,#2454,#1361,.T.);
#2939=EDGE_CURVE('',#2455,#2454,#1362,.T.);
#2940=EDGE_CURVE('',#2456,#2455,#1363,.T.);
#2941=EDGE_CURVE('',#2456,#2457,#1364,.T.);
#2942=EDGE_CURVE('',#2458,#2457,#1365,.T.);
#2943=EDGE_CURVE('',#2458,#2439,#1366,.T.);
#2944=EDGE_CURVE('',#2455,#2450,#1367,.T.);
#2945=EDGE_CURVE('',#2449,#2459,#1368,.T.);
#2946=EDGE_CURVE('',#2459,#2460,#235,.T.);
#2947=EDGE_CURVE('',#2460,#2456,#1369,.T.);
#2948=EDGE_CURVE('',#2461,#2459,#2213,.F.);
#2949=EDGE_CURVE('',#2461,#2446,#1370,.T.);
#2950=EDGE_CURVE('',#2462,#2461,#2214,.F.);
#2951=EDGE_CURVE('',#2463,#2462,#236,.T.);
#2952=EDGE_CURVE('',#2460,#2463,#2215,.F.);
#2953=EDGE_CURVE('',#2462,#2448,#1371,.T.);
#2954=EDGE_CURVE('',#2457,#2463,#1372,.T.);
#2955=EDGE_CURVE('',#2447,#2458,#1373,.T.);
#3738=ORIENTED_EDGE('',*,*,#2917,.F.);
#3739=ORIENTED_EDGE('',*,*,#2918,.F.);
#3740=ORIENTED_EDGE('',*,*,#2919,.F.);
#3741=ORIENTED_EDGE('',*,*,#2920,.F.);
#3742=ORIENTED_EDGE('',*,*,#2919,.T.);
#3743=ORIENTED_EDGE('',*,*,#2921,.T.);
#3744=ORIENTED_EDGE('',*,*,#2922,.F.);
#3745=ORIENTED_EDGE('',*,*,#2923,.F.);
#3746=ORIENTED_EDGE('',*,*,#2924,.T.);
#3747=ORIENTED_EDGE('',*,*,#2925,.T.);
#3748=ORIENTED_EDGE('',*,*,#2926,.T.);
#3749=ORIENTED_EDGE('',*,*,#2922,.T.);
#3750=ORIENTED_EDGE('',*,*,#2927,.T.);
#3751=ORIENTED_EDGE('',*,*,#2924,.F.);
#3752=ORIENTED_EDGE('',*,*,#2921,.F.);
#3753=ORIENTED_EDGE('',*,*,#2918,.T.);
#3754=ORIENTED_EDGE('',*,*,#2928,.F.);
#3755=ORIENTED_EDGE('',*,*,#2929,.F.);
#3756=ORIENTED_EDGE('',*,*,#2930,.T.);
#3757=ORIENTED_EDGE('',*,*,#2931,.F.);
#3758=ORIENTED_EDGE('',*,*,#2932,.T.);
#3759=ORIENTED_EDGE('',*,*,#2933,.T.);
#3760=ORIENTED_EDGE('',*,*,#2934,.T.);
#3761=ORIENTED_EDGE('',*,*,#2935,.T.);
#3762=ORIENTED_EDGE('',*,*,#2936,.T.);
#3763=ORIENTED_EDGE('',*,*,#2925,.F.);
#3764=ORIENTED_EDGE('',*,*,#2934,.F.);
#3765=ORIENTED_EDGE('',*,*,#2937,.F.);
#3766=ORIENTED_EDGE('',*,*,#2938,.F.);
#3767=ORIENTED_EDGE('',*,*,#2935,.F.);
#3768=ORIENTED_EDGE('',*,*,#2933,.F.);
#3769=ORIENTED_EDGE('',*,*,#2926,.F.);
#3770=ORIENTED_EDGE('',*,*,#2936,.F.);
#3771=ORIENTED_EDGE('',*,*,#2938,.T.);
#3772=ORIENTED_EDGE('',*,*,#2939,.F.);
#3773=ORIENTED_EDGE('',*,*,#2940,.F.);
#3774=ORIENTED_EDGE('',*,*,#2941,.T.);
#3775=ORIENTED_EDGE('',*,*,#2942,.F.);
#3776=ORIENTED_EDGE('',*,*,#2943,.T.);
#3777=ORIENTED_EDGE('',*,*,#2920,.T.);
#3778=ORIENTED_EDGE('',*,*,#2923,.T.);
#3779=ORIENTED_EDGE('',*,*,#2937,.T.);
#3780=ORIENTED_EDGE('',*,*,#2932,.F.);
#3781=ORIENTED_EDGE('',*,*,#2944,.F.);
#3782=ORIENTED_EDGE('',*,*,#2939,.T.);
#3783=ORIENTED_EDGE('',*,*,#2940,.T.);
#3784=ORIENTED_EDGE('',*,*,#2944,.T.);
#3785=ORIENTED_EDGE('',*,*,#2931,.T.);
#3786=ORIENTED_EDGE('',*,*,#2945,.T.);
#3787=ORIENTED_EDGE('',*,*,#2946,.T.);
#3788=ORIENTED_EDGE('',*,*,#2947,.T.);
#3789=ORIENTED_EDGE('',*,*,#2946,.F.);
#3790=ORIENTED_EDGE('',*,*,#2948,.F.);
#3791=ORIENTED_EDGE('',*,*,#2949,.T.);
#3792=ORIENTED_EDGE('',*,*,#2927,.F.);
#3793=ORIENTED_EDGE('',*,*,#2949,.F.);
#3794=ORIENTED_EDGE('',*,*,#2950,.F.);
#3795=ORIENTED_EDGE('',*,*,#2951,.F.);
#3796=ORIENTED_EDGE('',*,*,#2952,.F.);
#3797=ORIENTED_EDGE('',*,*,#2945,.F.);
#3798=ORIENTED_EDGE('',*,*,#2930,.F.);
#3799=ORIENTED_EDGE('',*,*,#2953,.F.);
#3800=ORIENTED_EDGE('',*,*,#2950,.T.);
#3801=ORIENTED_EDGE('',*,*,#2948,.T.);
#3802=ORIENTED_EDGE('',*,*,#2947,.F.);
#3803=ORIENTED_EDGE('',*,*,#2952,.T.);
#3804=ORIENTED_EDGE('',*,*,#2954,.F.);
#3805=ORIENTED_EDGE('',*,*,#2941,.F.);
#3806=ORIENTED_EDGE('',*,*,#2929,.T.);
#3807=ORIENTED_EDGE('',*,*,#2955,.T.);
#3808=ORIENTED_EDGE('',*,*,#2942,.T.);
#3809=ORIENTED_EDGE('',*,*,#2954,.T.);
#3810=ORIENTED_EDGE('',*,*,#2951,.T.);
#3811=ORIENTED_EDGE('',*,*,#2953,.T.);
#3812=ORIENTED_EDGE('',*,*,#2917,.T.);
#3813=ORIENTED_EDGE('',*,*,#2943,.F.);
#3814=ORIENTED_EDGE('',*,*,#2955,.F.);
#3815=ORIENTED_EDGE('',*,*,#2928,.T.);
#4639=CYLINDRICAL_SURFACE('',#5275,0.2117);
#4743=ADVANCED_FACE('',(#644),#432,.F.);
#4744=ADVANCED_FACE('',(#645),#433,.T.);
#4745=ADVANCED_FACE('',(#646,#335),#434,.T.);
#4746=ADVANCED_FACE('',(#647),#435,.T.);
#4747=ADVANCED_FACE('',(#648),#436,.T.);
#4748=ADVANCED_FACE('',(#649),#437,.F.);
#4749=ADVANCED_FACE('',(#650),#438,.T.);
#4750=ADVANCED_FACE('',(#651),#439,.T.);
#4751=ADVANCED_FACE('',(#652),#440,.T.);
#4752=ADVANCED_FACE('',(#653),#4639,.F.);
#4753=ADVANCED_FACE('',(#654),#441,.F.);
#4754=ADVANCED_FACE('',(#655),#442,.F.);
#4755=ADVANCED_FACE('',(#656),#443,.T.);
#4756=ADVANCED_FACE('',(#657),#444,.T.);
#4943=CLOSED_SHELL('',(#4743,#4744,#4745,#4746,#4747,#4748,#4749,#4750,
#4751,#4752,#4753,#4754,#4755,#4756));
#5263=AXIS2_PLACEMENT_3D('',#7455,#5992,#5993);
#5264=AXIS2_PLACEMENT_3D('',#7456,#5994,#5995);
#5265=AXIS2_PLACEMENT_3D('',#7465,#6000,#6001);
#5266=AXIS2_PLACEMENT_3D('',#7471,#6005,#6006);
#5267=AXIS2_PLACEMENT_3D('',#7478,#6010,#6011);
#5268=AXIS2_PLACEMENT_3D('',#7479,#6012,#6013);
#5269=AXIS2_PLACEMENT_3D('',#7493,#6021,#6022);
#5270=AXIS2_PLACEMENT_3D('',#7497,#6025,#6026);
#5271=AXIS2_PLACEMENT_3D('',#7501,#6029,#6030);
#5272=AXIS2_PLACEMENT_3D('',#7511,#6036,#6037);
#5273=AXIS2_PLACEMENT_3D('',#7513,#6039,#6040);
#5274=AXIS2_PLACEMENT_3D('',#7517,#6042,#6043);
#5275=AXIS2_PLACEMENT_3D('',#7519,#6045,#6046);
#5276=AXIS2_PLACEMENT_3D('',#7521,#6047,#6048);
#5277=AXIS2_PLACEMENT_3D('',#7524,#6050,#6051);
#5278=AXIS2_PLACEMENT_3D('',#7526,#6052,#6053);
#5279=AXIS2_PLACEMENT_3D('',#7527,#6054,#6055);
#5280=AXIS2_PLACEMENT_3D('',#7528,#6056,#6057);
#5281=AXIS2_PLACEMENT_3D('',#7530,#6059,#6060);
#5282=AXIS2_PLACEMENT_3D('',#7532,#6062,#6063);
#5283=AXIS2_PLACEMENT_3D('',#7534,#6065,#6066);
#5992=DIRECTION('axis',(0.,0.,1.));
#5993=DIRECTION('refdir',(1.,0.,0.));
#5994=DIRECTION('center_axis',(0.,0.,1.));
#5995=DIRECTION('ref_axis',(1.,0.,0.));
#5996=DIRECTION('',(1.,0.,0.));
#5997=DIRECTION('',(0.,-1.,0.));
#5998=DIRECTION('',(-1.,0.,0.));
#5999=DIRECTION('',(0.,1.,0.));
#6000=DIRECTION('center_axis',(0.,1.,0.));
#6001=DIRECTION('ref_axis',(-1.,0.,0.));
#6002=DIRECTION('',(0.,0.,1.));
#6003=DIRECTION('',(-1.,0.,0.));
#6004=DIRECTION('',(0.,0.,1.));
#6005=DIRECTION('center_axis',(0.,0.,1.));
#6006=DIRECTION('ref_axis',(1.,0.,0.));
#6007=DIRECTION('',(0.,-1.,0.));
#6008=DIRECTION('',(1.,0.,0.));
#6009=DIRECTION('',(0.,1.,0.));
#6010=DIRECTION('center_axis',(0.,0.,-1.));
#6011=DIRECTION('ref_axis',(1.,0.,0.));
#6012=DIRECTION('center_axis',(-1.,0.,0.));
#6013=DIRECTION('ref_axis',(0.,-1.,0.));
#6014=DIRECTION('',(0.,0.,1.));
#6015=DIRECTION('',(0.,0.707106781186548,0.707106781186548));
#6016=DIRECTION('',(0.,-1.,0.));
#6017=DIRECTION('',(0.,0.707106781186548,-0.707106781186548));
#6018=DIRECTION('',(0.,0.,1.));
#6019=DIRECTION('',(0.,-1.,0.));
#6020=DIRECTION('',(0.,0.,1.));
#6021=DIRECTION('center_axis',(0.,-1.,0.));
#6022=DIRECTION('ref_axis',(1.,0.,0.));
#6023=DIRECTION('',(1.,0.,0.));
#6024=DIRECTION('',(0.,0.,1.));
#6025=DIRECTION('center_axis',(0.,0.,1.));
#6026=DIRECTION('ref_axis',(1.,0.,0.));
#6027=DIRECTION('',(-1.,0.,0.));
#6028=DIRECTION('',(0.,1.,0.));
#6029=DIRECTION('center_axis',(1.,0.,0.));
#6030=DIRECTION('ref_axis',(0.,1.,0.));
#6031=DIRECTION('',(0.,0.,1.));
#6032=DIRECTION('',(0.,-0.707106781186548,0.707106781186548));
#6033=DIRECTION('',(0.,1.,0.));
#6034=DIRECTION('',(0.,-0.707106781186548,-0.707106781186548));
#6035=DIRECTION('',(0.,0.,1.));
#6036=DIRECTION('center_axis',(0.,-1.,0.));
#6037=DIRECTION('ref_axis',(1.,0.,0.));
#6038=DIRECTION('',(-1.,0.,0.));
#6039=DIRECTION('center_axis',(0.,-0.707106781186548,-0.707106781186548));
#6040=DIRECTION('ref_axis',(-1.,0.,0.));
#6041=DIRECTION('',(1.,0.,0.));
#6042=DIRECTION('center_axis',(0.,0.707106781186548,0.707106781186548));
#6043=DIRECTION('ref_axis',(0.,0.707106781186547,-0.707106781186547));
#6044=DIRECTION('',(1.,0.,0.));
#6045=DIRECTION('center_axis',(0.,0.,1.));
#6046=DIRECTION('ref_axis',(1.,0.,0.));
#6047=DIRECTION('center_axis',(0.,0.,-1.));
#6048=DIRECTION('ref_axis',(1.,0.,0.));
#6049=DIRECTION('',(0.,0.,1.));
#6050=DIRECTION('center_axis',(0.,0.,-1.));
#6051=DIRECTION('ref_axis',(1.,0.,0.));
#6052=DIRECTION('center_axis',(0.,-0.707106781186548,0.707106781186548));
#6053=DIRECTION('ref_axis',(0.,0.707106781186547,0.707106781186547));
#6054=DIRECTION('center_axis',(0.,0.,-1.));
#6055=DIRECTION('ref_axis',(1.,0.,0.));
#6056=DIRECTION('center_axis',(0.,0.,1.));
#6057=DIRECTION('ref_axis',(1.,0.,0.));
#6058=DIRECTION('',(-1.,0.,0.));
#6059=DIRECTION('center_axis',(0.,0.,1.));
#6060=DIRECTION('ref_axis',(1.,0.,0.));
#6061=DIRECTION('',(-1.,0.,0.));
#6062=DIRECTION('center_axis',(0.,0.707106781186548,-0.707106781186548));
#6063=DIRECTION('ref_axis',(-1.,0.,0.));
#6064=DIRECTION('',(1.,0.,0.));
#6065=DIRECTION('center_axis',(0.,1.,0.));
#6066=DIRECTION('ref_axis',(-1.,0.,0.));
#7455=CARTESIAN_POINT('',(0.,0.,0.));
#7456=CARTESIAN_POINT('Origin',(0.,0.395,0.25));
#7457=CARTESIAN_POINT('',(-0.5,0.3,0.25));
#7458=CARTESIAN_POINT('',(0.5,0.3,0.25));
#7459=CARTESIAN_POINT('',(0.25,0.3,0.25));
#7460=CARTESIAN_POINT('',(-0.5,0.5,0.25));
#7461=CARTESIAN_POINT('',(-0.5,0.5,0.25));
#7462=CARTESIAN_POINT('',(0.5,0.5,0.25));
#7463=CARTESIAN_POINT('',(0.5,0.5,0.25));
#7464=CARTESIAN_POINT('',(0.5,0.29,0.25));
#7465=CARTESIAN_POINT('Origin',(0.5,0.5,0.25));
#7466=CARTESIAN_POINT('',(-0.5,0.5,0.4));
#7467=CARTESIAN_POINT('',(-0.5,0.5,0.25));
#7468=CARTESIAN_POINT('',(0.5,0.5,0.4));
#7469=CARTESIAN_POINT('',(0.5,0.5,0.4));
#7470=CARTESIAN_POINT('',(0.5,0.5,0.25));
#7471=CARTESIAN_POINT('Origin',(0.,0.,0.4));
#7472=CARTESIAN_POINT('',(-0.5,-0.5,0.4));
#7473=CARTESIAN_POINT('',(-0.5,0.5,0.4));
#7474=CARTESIAN_POINT('',(0.5,-0.5,0.4));
#7475=CARTESIAN_POINT('',(-0.5,-0.5,0.4));
#7476=CARTESIAN_POINT('',(0.5,-0.3,0.4));
#7477=CARTESIAN_POINT('',(-0.2117,2.59257727379495E-17,0.4));
#7478=CARTESIAN_POINT('Origin',(0.,0.,0.4));
#7479=CARTESIAN_POINT('Origin',(-0.5,0.3,0.));
#7480=CARTESIAN_POINT('',(-0.5,0.3,0.15));
#7481=CARTESIAN_POINT('',(-0.5,0.3,0.));
#7482=CARTESIAN_POINT('',(-0.5,0.15,0.));
#7483=CARTESIAN_POINT('',(-0.5,0.225,0.075));
#7484=CARTESIAN_POINT('',(-0.5,-0.15,0.));
#7485=CARTESIAN_POINT('',(-0.5,0.3,0.));
#7486=CARTESIAN_POINT('',(-0.5,-0.3,0.15));
#7487=CARTESIAN_POINT('',(-0.5,-0.075,-0.075));
#7488=CARTESIAN_POINT('',(-0.5,-0.3,0.25));
#7489=CARTESIAN_POINT('',(-0.5,-0.3,0.));
#7490=CARTESIAN_POINT('',(-0.5,-0.5,0.25));
#7491=CARTESIAN_POINT('',(-0.5,-0.29,0.25));
#7492=CARTESIAN_POINT('',(-0.5,-0.5,0.25));
#7493=CARTESIAN_POINT('Origin',(-0.5,-0.5,0.25));
#7494=CARTESIAN_POINT('',(0.5,-0.5,0.25));
#7495=CARTESIAN_POINT('',(-0.5,-0.5,0.25));
#7496=CARTESIAN_POINT('',(0.5,-0.5,0.25));
#7497=CARTESIAN_POINT('Origin',(0.,-0.395,0.25));
#7498=CARTESIAN_POINT('',(0.5,-0.3,0.25));
#7499=CARTESIAN_POINT('',(-0.25,-0.3,0.25));
#7500=CARTESIAN_POINT('',(0.5,-0.5,0.25));
#7501=CARTESIAN_POINT('Origin',(0.5,-0.3,0.));
#7502=CARTESIAN_POINT('',(0.5,-0.3,0.15));
#7503=CARTESIAN_POINT('',(0.5,-0.3,0.));
#7504=CARTESIAN_POINT('',(0.5,-0.15,0.));
#7505=CARTESIAN_POINT('',(0.5,-0.225,0.075));
#7506=CARTESIAN_POINT('',(0.5,0.15,0.));
#7507=CARTESIAN_POINT('',(0.5,-0.3,0.));
#7508=CARTESIAN_POINT('',(0.5,0.3,0.15));
#7509=CARTESIAN_POINT('',(0.5,0.075,-0.075));
#7510=CARTESIAN_POINT('',(0.5,0.3,0.));
#7511=CARTESIAN_POINT('Origin',(-0.5,-0.3,0.));
#7512=CARTESIAN_POINT('',(-0.25,-0.3,0.15));
#7513=CARTESIAN_POINT('Origin',(-0.25,-0.225,0.075));
#7514=CARTESIAN_POINT('',(-0.149388386429468,-0.15,0.));
#7515=CARTESIAN_POINT('',(-0.25,-0.15,0.));
#7516=CARTESIAN_POINT('',(0.149388386429468,-0.15,0.));
#7517=CARTESIAN_POINT('Origin',(0.,0.,-0.15));
#7518=CARTESIAN_POINT('',(-0.25,-0.15,0.));
#7519=CARTESIAN_POINT('Origin',(0.,0.,-0.1));
#7520=CARTESIAN_POINT('',(-0.2117,-2.59257727379495E-17,0.));
#7521=CARTESIAN_POINT('Origin',(0.,0.,0.));
#7522=CARTESIAN_POINT('',(-0.2117,-2.59257727379495E-17,-0.1));
#7523=CARTESIAN_POINT('',(-0.149388386429468,0.15,0.));
#7524=CARTESIAN_POINT('Origin',(0.,0.,0.));
#7525=CARTESIAN_POINT('',(0.149388386429468,0.15,0.));
#7526=CARTESIAN_POINT('Origin',(0.,0.,-0.15));
#7527=CARTESIAN_POINT('Origin',(0.,0.,0.));
#7528=CARTESIAN_POINT('Origin',(0.,0.,0.));
#7529=CARTESIAN_POINT('',(0.25,0.15,0.));
#7530=CARTESIAN_POINT('Origin',(0.,0.,0.));
#7531=CARTESIAN_POINT('',(0.25,0.15,0.));
#7532=CARTESIAN_POINT('Origin',(0.25,0.225,0.075));
#7533=CARTESIAN_POINT('',(0.25,0.3,0.15));
#7534=CARTESIAN_POINT('Origin',(0.5,0.3,0.));
#8458=UNCERTAINTY_MEASURE_WITH_UNIT(LENGTH_MEASURE(0.001),#8500,
'DISTANCE_ACCURACY_VALUE',
'Maximum model space distance between geometric entities at asserted c
onnectivities');
#8476=UNCERTAINTY_MEASURE_WITH_UNIT(LENGTH_MEASURE(0.001),#8500,
'DISTANCE_ACCURACY_VALUE',
'Maximum model space distance between geometric entities at asserted c
onnectivities');
#8481=(
GEOMETRIC_REPRESENTATION_CONTEXT(3)
GLOBAL_UNCERTAINTY_ASSIGNED_CONTEXT((#8458))
GLOBAL_UNIT_ASSIGNED_CONTEXT((#8500,#8502,#8503))
REPRESENTATION_CONTEXT('','3D')
);
#8499=(
GEOMETRIC_REPRESENTATION_CONTEXT(3)
GLOBAL_UNCERTAINTY_ASSIGNED_CONTEXT((#8476))
GLOBAL_UNIT_ASSIGNED_CONTEXT((#8500,#8502,#8503))
REPRESENTATION_CONTEXT('','3D')
);
#8500=(
LENGTH_UNIT()
NAMED_UNIT(*)
SI_UNIT(.CENTI.,.METRE.)
);
#8502=(
NAMED_UNIT(*)
PLANE_ANGLE_UNIT()
SI_UNIT($,.RADIAN.)
);
#8503=(
NAMED_UNIT(*)
SI_UNIT($,.STERADIAN.)
SOLID_ANGLE_UNIT()
);
#8508=SHAPE_DEFINITION_REPRESENTATION(#8530,#8602);
#8530=PRODUCT_DEFINITION_SHAPE('',$,#8625);
#8602=SHAPE_REPRESENTATION('',(#5263),#8481);
#8620=PRODUCT_DEFINITION_CONTEXT('part definition',#8688,'design');
#8625=PRODUCT_DEFINITION('Captive slot nut','Captive slot nut',#8647,#8620);
#8647=PRODUCT_DEFINITION_FORMATION('',$,#8694);
#8688=APPLICATION_CONTEXT(
'Core Data for Automotive Mechanical Design Process');
#8689=PRODUCT_CONTEXT('part definition',#8688,'mechanical');
#8694=PRODUCT('Captive slot nut','Captive slot nut','Captive slot nut',
(#8689));
#8789=COLOUR_RGB('Black',0.12,0.14,0.17);
#8790=FILL_AREA_STYLE_COLOUR('',#8789);
#8791=FILL_AREA_STYLE('',(#8790));
#8792=SURFACE_STYLE_FILL_AREA(#8791);
#8793=SURFACE_SIDE_STYLE('',(#8792));
#8794=SURFACE_STYLE_USAGE(.BOTH.,#8793);
#8795=PRESENTATION_STYLE_ASSIGNMENT((#8794));
ENDSEC;
END-ISO-10303-21;
